ISO-10303-21;
HEADER;
/* Generated by software containing ST-Developer
 * from STEP Tools, Inc. (www.steptools.com) 
 */

FILE_DESCRIPTION(
/* description */ ('Fatigue rig crank-slider'),
/* implementation_level */ '2;1');

FILE_NAME(
/* name */ 'Socket Set Screw - M5x8.step',
/* time_stamp */ '2026-10-28T03:24:50-07:00',
/* author */ (''),
/* organization */ (''),
/* preprocessor_version */ 'ST-DEVELOPER v20.2',
/* originating_system */ 'Autodesk Translation Framework v15.17.0.0',
/* authorisation */ '');

FILE_SCHEMA (('AUTOMOTIVE_DESIGN { 1 0 10303 214 3 1 1 }'));
ENDSEC;

DATA;
#10=MECHANICAL_DESIGN_GEOMETRIC_PRESENTATION_REPRESENTATION('',(#614),#16911);
#20=CONICAL_SURFACE('',#10045,0.235,0.785398163397448);
#21=CONICAL_SURFACE('',#10049,0.2125,0.785398163397448);
#513=SHAPE_REPRESENTATION_RELATIONSHIP('SRR','None',#17154,#563);
#563=ADVANCED_BREP_SHAPE_REPRESENTATION('',(#671),#16883);
#614=STYLED_ITEM('',(#17494),#671);
#671=MANIFOLD_SOLID_BREP('Body1',#8907);
#841=FACE_BOUND('',#2178,.T.);
#1073=PLANE('',#10036);
#1074=PLANE('',#10037);
#1075=PLANE('',#10038);
#1076=PLANE('',#10039);
#1077=PLANE('',#10040);
#1078=PLANE('',#10041);
#1079=PLANE('',#10042);
#1080=PLANE('',#10043);
#1081=PLANE('',#10051);
#1506=FACE_OUTER_BOUND('',#2170,.T.);
#1507=FACE_OUTER_BOUND('',#2171,.T.);
#1508=FACE_OUTER_BOUND('',#2172,.T.);
#1509=FACE_OUTER_BOUND('',#2173,.T.);
#1510=FACE_OUTER_BOUND('',#2174,.T.);
#1511=FACE_OUTER_BOUND('',#2175,.T.);
#1512=FACE_OUTER_BOUND('',#2176,.T.);
#1513=FACE_OUTER_BOUND('',#2177,.T.);
#1514=FACE_OUTER_BOUND('',#2179,.T.);
#1515=FACE_OUTER_BOUND('',#2180,.T.);
#1516=FACE_OUTER_BOUND('',#2181,.T.);
#1517=FACE_OUTER_BOUND('',#2182,.T.);
#2170=EDGE_LOOP('',(#7206,#7207,#7208,#7209));
#2171=EDGE_LOOP('',(#7210,#7211,#7212,#7213));
#2172=EDGE_LOOP('',(#7214,#7215,#7216,#7217));
#2173=EDGE_LOOP('',(#7218,#7219,#7220,#7221));
#2174=EDGE_LOOP('',(#7222,#7223,#7224,#7225));
#2175=EDGE_LOOP('',(#7226,#7227,#7228,#7229));
#2176=EDGE_LOOP('',(#7230,#7231,#7232,#7233,#7234,#7235));
#2177=EDGE_LOOP('',(#7236));
#2178=EDGE_LOOP('',(#7237,#7238,#7239,#7240,#7241,#7242));
#2179=EDGE_LOOP('',(#7243,#7244,#7245,#7246));
#2180=EDGE_LOOP('',(#7247,#7248,#7249,#7250));
#2181=EDGE_LOOP('',(#7251,#7252,#7253,#7254));
#2182=EDGE_LOOP('',(#7255));
#2808=LINE('',#15278,#3454);
#2809=LINE('',#15280,#3455);
#2810=LINE('',#15282,#3456);
#2811=LINE('',#15283,#3457);
#2812=LINE('',#15286,#3458);
#2813=LINE('',#15288,#3459);
#2814=LINE('',#15289,#3460);
#2815=LINE('',#15292,#3461);
#2816=LINE('',#15294,#3462);
#2817=LINE('',#15295,#3463);
#2818=LINE('',#15298,#3464);
#2819=LINE('',#15300,#3465);
#2820=LINE('',#15301,#3466);
#2821=LINE('',#15304,#3467);
#2822=LINE('',#15306,#3468);
#2823=LINE('',#15307,#3469);
#2824=LINE('',#15309,#3470);
#2825=LINE('',#15310,#3471);
#2826=LINE('',#15318,#3472);
#2827=LINE('',#15322,#3473);
#2828=LINE('',#15326,#3474);
#3454=VECTOR('',#12002,1.);
#3455=VECTOR('',#12003,1.);
#3456=VECTOR('',#12004,1.);
#3457=VECTOR('',#12005,1.);
#3458=VECTOR('',#12008,1.);
#3459=VECTOR('',#12009,1.);
#3460=VECTOR('',#12010,1.);
#3461=VECTOR('',#12013,1.);
#3462=VECTOR('',#12014,1.);
#3463=VECTOR('',#12015,1.);
#3464=VECTOR('',#12018,1.);
#3465=VECTOR('',#12019,1.);
#3466=VECTOR('',#12020,1.);
#3467=VECTOR('',#12023,1.);
#3468=VECTOR('',#12024,1.);
#3469=VECTOR('',#12025,1.);
#3470=VECTOR('',#12028,1.);
#3471=VECTOR('',#12029,1.);
#3472=VECTOR('',#12040,0.235);
#3473=VECTOR('',#12045,0.25);
#3474=VECTOR('',#12050,0.2125);
#3973=CIRCLE('',#10044,0.22);
#3974=CIRCLE('',#10046,0.24505);
#3975=CIRCLE('',#10048,0.24505);
#3976=CIRCLE('',#10050,0.175);
#4561=VERTEX_POINT('',#15276);
#4562=VERTEX_POINT('',#15277);
#4563=VERTEX_POINT('',#15279);
#4564=VERTEX_POINT('',#15281);
#4565=VERTEX_POINT('',#15285);
#4566=VERTEX_POINT('',#15287);
#4567=VERTEX_POINT('',#15291);
#4568=VERTEX_POINT('',#15293);
#4569=VERTEX_POINT('',#15297);
#4570=VERTEX_POINT('',#15299);
#4571=VERTEX_POINT('',#15303);
#4572=VERTEX_POINT('',#15305);
#4573=VERTEX_POINT('',#15313);
#4574=VERTEX_POINT('',#15316);
#4575=VERTEX_POINT('',#15320);
#4576=VERTEX_POINT('',#15324);
#5501=EDGE_CURVE('',#4561,#4562,#2808,.T.);
#5502=EDGE_CURVE('',#4561,#4563,#2809,.T.);
#5503=EDGE_CURVE('',#4563,#4564,#2810,.T.);
#5504=EDGE_CURVE('',#4562,#4564,#2811,.T.);
#5505=EDGE_CURVE('',#4565,#4561,#2812,.T.);
#5506=EDGE_CURVE('',#4565,#4566,#2813,.T.);
#5507=EDGE_CURVE('',#4566,#4563,#2814,.T.);
#5508=EDGE_CURVE('',#4567,#4565,#2815,.T.);
#5509=EDGE_CURVE('',#4567,#4568,#2816,.T.);
#5510=EDGE_CURVE('',#4568,#4566,#2817,.T.);
#5511=EDGE_CURVE('',#4569,#4567,#2818,.T.);
#5512=EDGE_CURVE('',#4569,#4570,#2819,.T.);
#5513=EDGE_CURVE('',#4570,#4568,#2820,.T.);
#5514=EDGE_CURVE('',#4571,#4569,#2821,.T.);
#5515=EDGE_CURVE('',#4571,#4572,#2822,.T.);
#5516=EDGE_CURVE('',#4572,#4570,#2823,.T.);
#5517=EDGE_CURVE('',#4562,#4571,#2824,.T.);
#5518=EDGE_CURVE('',#4564,#4572,#2825,.T.);
#5519=EDGE_CURVE('',#4573,#4573,#3973,.T.);
#5520=EDGE_CURVE('',#4574,#4574,#3974,.T.);
#5521=EDGE_CURVE('',#4574,#4573,#2826,.T.);
#5522=EDGE_CURVE('',#4575,#4575,#3975,.F.);
#5523=EDGE_CURVE('',#4575,#4574,#2827,.T.);
#5524=EDGE_CURVE('',#4576,#4576,#3976,.T.);
#5525=EDGE_CURVE('',#4576,#4575,#2828,.T.);
#7206=ORIENTED_EDGE('',*,*,#5501,.F.);
#7207=ORIENTED_EDGE('',*,*,#5502,.T.);
#7208=ORIENTED_EDGE('',*,*,#5503,.T.);
#7209=ORIENTED_EDGE('',*,*,#5504,.F.);
#7210=ORIENTED_EDGE('',*,*,#5505,.F.);
#7211=ORIENTED_EDGE('',*,*,#5506,.T.);
#7212=ORIENTED_EDGE('',*,*,#5507,.T.);
#7213=ORIENTED_EDGE('',*,*,#5502,.F.);
#7214=ORIENTED_EDGE('',*,*,#5508,.F.);
#7215=ORIENTED_EDGE('',*,*,#5509,.T.);
#7216=ORIENTED_EDGE('',*,*,#5510,.T.);
#7217=ORIENTED_EDGE('',*,*,#5506,.F.);
#7218=ORIENTED_EDGE('',*,*,#5511,.F.);
#7219=ORIENTED_EDGE('',*,*,#5512,.T.);
#7220=ORIENTED_EDGE('',*,*,#5513,.T.);
#7221=ORIENTED_EDGE('',*,*,#5509,.F.);
#7222=ORIENTED_EDGE('',*,*,#5514,.F.);
#7223=ORIENTED_EDGE('',*,*,#5515,.T.);
#7224=ORIENTED_EDGE('',*,*,#5516,.T.);
#7225=ORIENTED_EDGE('',*,*,#5512,.F.);
#7226=ORIENTED_EDGE('',*,*,#5517,.F.);
#7227=ORIENTED_EDGE('',*,*,#5504,.T.);
#7228=ORIENTED_EDGE('',*,*,#5518,.T.);
#7229=ORIENTED_EDGE('',*,*,#5515,.F.);
#7230=ORIENTED_EDGE('',*,*,#5518,.F.);
#7231=ORIENTED_EDGE('',*,*,#5503,.F.);
#7232=ORIENTED_EDGE('',*,*,#5507,.F.);
#7233=ORIENTED_EDGE('',*,*,#5510,.F.);
#7234=ORIENTED_EDGE('',*,*,#5513,.F.);
#7235=ORIENTED_EDGE('',*,*,#5516,.F.);
#7236=ORIENTED_EDGE('',*,*,#5519,.F.);
#7237=ORIENTED_EDGE('',*,*,#5501,.T.);
#7238=ORIENTED_EDGE('',*,*,#5517,.T.);
#7239=ORIENTED_EDGE('',*,*,#5514,.T.);
#7240=ORIENTED_EDGE('',*,*,#5511,.T.);
#7241=ORIENTED_EDGE('',*,*,#5508,.T.);
#7242=ORIENTED_EDGE('',*,*,#5505,.T.);
#7243=ORIENTED_EDGE('',*,*,#5520,.F.);
#7244=ORIENTED_EDGE('',*,*,#5521,.T.);
#7245=ORIENTED_EDGE('',*,*,#5519,.T.);
#7246=ORIENTED_EDGE('',*,*,#5521,.F.);
#7247=ORIENTED_EDGE('',*,*,#5522,.F.);
#7248=ORIENTED_EDGE('',*,*,#5523,.T.);
#7249=ORIENTED_EDGE('',*,*,#5520,.T.);
#7250=ORIENTED_EDGE('',*,*,#5523,.F.);
#7251=ORIENTED_EDGE('',*,*,#5524,.F.);
#7252=ORIENTED_EDGE('',*,*,#5525,.T.);
#7253=ORIENTED_EDGE('',*,*,#5522,.T.);
#7254=ORIENTED_EDGE('',*,*,#5525,.F.);
#7255=ORIENTED_EDGE('',*,*,#5524,.T.);
#8300=CYLINDRICAL_SURFACE('',#10047,0.24505);
#8644=ADVANCED_FACE('',(#1506),#1073,.F.);
#8645=ADVANCED_FACE('',(#1507),#1074,.F.);
#8646=ADVANCED_FACE('',(#1508),#1075,.F.);
#8647=ADVANCED_FACE('',(#1509),#1076,.F.);
#8648=ADVANCED_FACE('',(#1510),#1077,.F.);
#8649=ADVANCED_FACE('',(#1511),#1078,.F.);
#8650=ADVANCED_FACE('',(#1512),#1079,.F.);
#8651=ADVANCED_FACE('',(#1513,#841),#1080,.T.);
#8652=ADVANCED_FACE('',(#1514),#20,.T.);
#8653=ADVANCED_FACE('',(#1515),#8300,.T.);
#8654=ADVANCED_FACE('',(#1516),#21,.T.);
#8655=ADVANCED_FACE('',(#1517),#1081,.T.);
#8907=CLOSED_SHELL('',(#8644,#8645,#8646,#8647,#8648,#8649,#8650,#8651,
#8652,#8653,#8654,#8655));
#10035=AXIS2_PLACEMENT_3D('',#15274,#11998,#11999);
#10036=AXIS2_PLACEMENT_3D('',#15275,#12000,#12001);
#10037=AXIS2_PLACEMENT_3D('',#15284,#12006,#12007);
#10038=AXIS2_PLACEMENT_3D('',#15290,#12011,#12012);
#10039=AXIS2_PLACEMENT_3D('',#15296,#12016,#12017);
#10040=AXIS2_PLACEMENT_3D('',#15302,#12021,#12022);
#10041=AXIS2_PLACEMENT_3D('',#15308,#12026,#12027);
#10042=AXIS2_PLACEMENT_3D('',#15311,#12030,#12031);
#10043=AXIS2_PLACEMENT_3D('',#15312,#12032,#12033);
#10044=AXIS2_PLACEMENT_3D('',#15314,#12034,#12035);
#10045=AXIS2_PLACEMENT_3D('',#15315,#12036,#12037);
#10046=AXIS2_PLACEMENT_3D('',#15317,#12038,#12039);
#10047=AXIS2_PLACEMENT_3D('',#15319,#12041,#12042);
#10048=AXIS2_PLACEMENT_3D('',#15321,#12043,#12044);
#10049=AXIS2_PLACEMENT_3D('',#15323,#12046,#12047);
#10050=AXIS2_PLACEMENT_3D('',#15325,#12048,#12049);
#10051=AXIS2_PLACEMENT_3D('',#15327,#12051,#12052);
#11998=DIRECTION('axis',(0.,0.,1.));
#11999=DIRECTION('refdir',(1.,0.,0.));
#12000=DIRECTION('center_axis',(0.866025403784439,0.,-0.5));
#12001=DIRECTION('ref_axis',(0.5,0.,0.866025403784439));
#12002=DIRECTION('',(0.5,0.,0.866025403784439));
#12003=DIRECTION('',(0.,-1.,0.));
#12004=DIRECTION('',(0.5,0.,0.866025403784439));
#12005=DIRECTION('',(0.,-1.,0.));
#12006=DIRECTION('center_axis',(1.92296268638356E-16,0.,-1.));
#12007=DIRECTION('ref_axis',(1.,0.,1.92296268638356E-16));
#12008=DIRECTION('',(1.,0.,1.92296268638356E-16));
#12009=DIRECTION('',(0.,-1.,0.));
#12010=DIRECTION('',(1.,0.,1.92296268638356E-16));
#12011=DIRECTION('center_axis',(-0.866025403784439,0.,-0.5));
#12012=DIRECTION('ref_axis',(0.5,0.,-0.866025403784439));
#12013=DIRECTION('',(0.5,0.,-0.866025403784439));
#12014=DIRECTION('',(0.,-1.,0.));
#12015=DIRECTION('',(0.5,0.,-0.866025403784438));
#12016=DIRECTION('center_axis',(-0.866025403784439,0.,0.5));
#12017=DIRECTION('ref_axis',(-0.5,0.,-0.866025403784439));
#12018=DIRECTION('',(-0.5,0.,-0.866025403784439));
#12019=DIRECTION('',(0.,-1.,0.));
#12020=DIRECTION('',(-0.5,0.,-0.866025403784439));
#12021=DIRECTION('center_axis',(-1.92296268638356E-16,0.,1.));
#12022=DIRECTION('ref_axis',(-1.,0.,-1.92296268638356E-16));
#12023=DIRECTION('',(-1.,0.,-1.92296268638356E-16));
#12024=DIRECTION('',(0.,-1.,0.));
#12025=DIRECTION('',(-1.,0.,-1.92296268638356E-16));
#12026=DIRECTION('center_axis',(0.866025403784439,0.,0.5));
#12027=DIRECTION('ref_axis',(-0.5,0.,0.866025403784439));
#12028=DIRECTION('',(-0.5,0.,0.866025403784439));
#12029=DIRECTION('',(-0.5,0.,0.866025403784439));
#12030=DIRECTION('center_axis',(0.,-1.,0.));
#12031=DIRECTION('ref_axis',(0.,0.,-1.));
#12032=DIRECTION('center_axis',(0.,1.,0.));
#12033=DIRECTION('ref_axis',(0.,0.,1.));
#12034=DIRECTION('center_axis',(0.,-1.,0.));
#12035=DIRECTION('ref_axis',(1.,0.,0.));
#12036=DIRECTION('center_axis',(0.,-1.,0.));
#12037=DIRECTION('ref_axis',(1.,0.,0.));
#12038=DIRECTION('center_axis',(0.,-1.,0.));
#12039=DIRECTION('ref_axis',(1.,0.,0.));
#12040=DIRECTION('',(0.707106781186547,0.707106781186548,8.65956056235493E-17));
#12041=DIRECTION('center_axis',(0.,-1.,0.));
#12042=DIRECTION('ref_axis',(1.,0.,0.));
#12043=DIRECTION('center_axis',(0.,1.,0.));
#12044=DIRECTION('ref_axis',(1.,0.,0.));
#12045=DIRECTION('',(0.,1.,0.));
#12046=DIRECTION('center_axis',(0.,1.,0.));
#12047=DIRECTION('ref_axis',(1.,0.,0.));
#12048=DIRECTION('center_axis',(0.,-1.,0.));
#12049=DIRECTION('ref_axis',(1.,0.,0.));
#12050=DIRECTION('',(-0.707106781186547,0.707106781186548,-8.65956056235493E-17));
#12051=DIRECTION('center_axis',(0.,-1.,0.));
#12052=DIRECTION('ref_axis',(0.,0.,-1.));
#15274=CARTESIAN_POINT('',(0.,0.,0.));
#15275=CARTESIAN_POINT('Origin',(0.0721687836487032,0.,-0.125));
#15276=CARTESIAN_POINT('',(0.0721687836487032,0.,-0.125));
#15277=CARTESIAN_POINT('',(0.144337567297406,0.,0.));
#15278=CARTESIAN_POINT('',(0.117710979560879,0.,-0.0461186027918559));
#15279=CARTESIAN_POINT('',(0.0721687836487032,-0.25,-0.125));
#15280=CARTESIAN_POINT('',(0.0721687836487032,0.,-0.125));
#15281=CARTESIAN_POINT('',(0.144337567297406,-0.25,0.));
#15282=CARTESIAN_POINT('',(0.144337567297406,-0.25,0.));
#15283=CARTESIAN_POINT('',(0.144337567297406,0.,0.));
#15284=CARTESIAN_POINT('Origin',(-0.0721687836487032,0.,-0.125));
#15285=CARTESIAN_POINT('',(-0.0721687836487032,0.,-0.125));
#15286=CARTESIAN_POINT('',(0.0739156081756484,0.,-0.125));
#15287=CARTESIAN_POINT('',(-0.0721687836487032,-0.25,-0.125));
#15288=CARTESIAN_POINT('',(-0.0721687836487032,0.,-0.125));
#15289=CARTESIAN_POINT('',(0.0721687836487032,-0.25,-0.125));
#15290=CARTESIAN_POINT('Origin',(-0.144337567297406,0.,-4.16333634234434E-17));
#15291=CARTESIAN_POINT('',(-0.144337567297406,0.,-1.76762539787485E-17));
#15292=CARTESIAN_POINT('',(-0.0987953713852306,0.,-0.0788813972081442));
#15293=CARTESIAN_POINT('',(-0.144337567297406,-0.25,-2.77555756156289E-17));
#15294=CARTESIAN_POINT('',(-0.144337567297406,0.,-1.76762539787485E-17));
#15295=CARTESIAN_POINT('',(-0.0721687836487032,-0.25,-0.125));
#15296=CARTESIAN_POINT('Origin',(-0.0721687836487033,0.,0.125));
#15297=CARTESIAN_POINT('',(-0.0721687836487033,0.,0.125));
#15298=CARTESIAN_POINT('',(-0.0627109795608791,0.,0.141381397208144));
#15299=CARTESIAN_POINT('',(-0.0721687836487033,-0.25,0.125));
#15300=CARTESIAN_POINT('',(-0.0721687836487033,0.,0.125));
#15301=CARTESIAN_POINT('',(-0.144337567297406,-0.25,-1.76762539787485E-17));
#15302=CARTESIAN_POINT('Origin',(0.0721687836487032,0.,0.125));
#15303=CARTESIAN_POINT('',(0.0721687836487032,0.,0.125));
#15304=CARTESIAN_POINT('',(0.146084391824352,0.,0.125));
#15305=CARTESIAN_POINT('',(0.0721687836487032,-0.25,0.125));
#15306=CARTESIAN_POINT('',(0.0721687836487032,0.,0.125));
#15307=CARTESIAN_POINT('',(-0.0721687836487033,-0.25,0.125));
#15308=CARTESIAN_POINT('Origin',(0.144337567297406,0.,0.));
#15309=CARTESIAN_POINT('',(0.153795371385231,0.,-0.0163813972081441));
#15310=CARTESIAN_POINT('',(0.0721687836487032,-0.25,0.125));
#15311=CARTESIAN_POINT('Origin',(0.,-0.25,0.));
#15312=CARTESIAN_POINT('Origin',(0.22,0.,0.));
#15313=CARTESIAN_POINT('',(-0.22,-8.67361737988404E-18,-2.69422295812418E-17));
#15314=CARTESIAN_POINT('Origin',(0.,0.,0.));
#15315=CARTESIAN_POINT('Origin',(0.,-0.015,0.));
#15316=CARTESIAN_POINT('',(-0.24505,-0.02505,-3.00099698131059E-17));
#15317=CARTESIAN_POINT('Origin',(0.,-0.02505,0.));
#15318=CARTESIAN_POINT('',(-0.235,-0.015,-2.87791997799628E-17));
#15319=CARTESIAN_POINT('Origin',(0.,-0.3775,0.));
#15320=CARTESIAN_POINT('',(-0.24505,-0.72995,3.00099698131059E-17));
#15321=CARTESIAN_POINT('Origin',(0.,-0.72995,0.));
#15322=CARTESIAN_POINT('',(-0.24505,-0.3775,-3.00099698131059E-17));
#15323=CARTESIAN_POINT('Origin',(0.,-0.7625,0.));
#15324=CARTESIAN_POINT('',(-0.175,-0.8,-2.14313189850787E-17));
#15325=CARTESIAN_POINT('Origin',(0.,-0.8,0.));
#15326=CARTESIAN_POINT('',(-0.2125,-0.7625,-2.60237444818813E-17));
#15327=CARTESIAN_POINT('Origin',(0.,-0.8,0.));
#16824=UNCERTAINTY_MEASURE_WITH_UNIT(LENGTH_MEASURE(0.001),#16912,
'DISTANCE_ACCURACY_VALUE',
'Maximum model space distance between geometric entities at asserted c
onnectivities');
#16852=UNCERTAINTY_MEASURE_WITH_UNIT(LENGTH_MEASURE(0.001),#16912,
'DISTANCE_ACCURACY_VALUE',
'Maximum model space distance between geometric entities at asserted c
onnectivities');
#16883=(
GEOMETRIC_REPRESENTATION_CONTEXT(3)
GLOBAL_UNCERTAINTY_ASSIGNED_CONTEXT((#16824))
GLOBAL_UNIT_ASSIGNED_CONTEXT((#16912,#16914,#16915))
REPRESENTATION_CONTEXT('','3D')
);
#16911=(
GEOMETRIC_REPRESENTATION_CONTEXT(3)
GLOBAL_UNCERTAINTY_ASSIGNED_CONTEXT((#16852))
GLOBAL_UNIT_ASSIGNED_CONTEXT((#16912,#16914,#16915))
REPRESENTATION_CONTEXT('','3D')
);
#16912=(
LENGTH_UNIT()
NAMED_UNIT(*)
SI_UNIT(.CENTI.,.METRE.)
);
#16914=(
NAMED_UNIT(*)
PLANE_ANGLE_UNIT()
SI_UNIT($,.RADIAN.)
);
#16915=(
NAMED_UNIT(*)
SI_UNIT($,.STERADIAN.)
SOLID_ANGLE_UNIT()
);
#16946=SHAPE_DEFINITION_REPRESENTATION(#17006,#17154);
#17006=PRODUCT_DEFINITION_SHAPE('',$,#17213);
#17154=SHAPE_REPRESENTATION('',(#10035),#16883);
#17182=PRODUCT_DEFINITION_CONTEXT('part definition',#17358,'design');
#17213=PRODUCT_DEFINITION('Socket Set Screw - M5x8',
'Socket Set Screw - M5x8',#17271,#17182);
#17271=PRODUCT_DEFINITION_FORMATION('',$,#17390);
#17358=APPLICATION_CONTEXT(
'Core Data for Automotive Mechanical Design Process');
#17359=PRODUCT_CONTEXT('part definition',#17358,'mechanical');
#17390=PRODUCT('Socket Set Screw - M5x8','Socket Set Screw - M5x8',
'Socket Set Screw - M5x8',(#17359));
#17488=COLOUR_RGB('Black',0.12,0.14,0.17);
#17489=FILL_AREA_STYLE_COLOUR('',#17488);
#17490=FILL_AREA_STYLE('',(#17489));
#17491=SURFACE_STYLE_FILL_AREA(#17490);
#17492=SURFACE_SIDE_STYLE('',(#17491));
#17493=SURFACE_STYLE_USAGE(.BOTH.,#17492);
#17494=PRESENTATION_STYLE_ASSIGNMENT((#17493));
ENDSEC;
END-ISO-10303-21;
